ISO-10303-21;
HEADER;
/* Generated by software containing ST-Developer
 * from STEP Tools, Inc. (www.steptools.com) 
 */

FILE_DESCRIPTION(
/* description */ ('STEP AP203'),
/* implementation_level */ '2;1');

FILE_NAME(
/* name */ 'F06_M4x10_Retainer_Screw.step',
/* time_stamp */ '2026-11-15T15:04:01-08:00',
/* author */ (''),
/* organization */ (''),
/* preprocessor_version */ 'ST-DEVELOPER v20.2',
/* originating_system */ 'Autodesk Translation Framework v15.17.0.0',
/* authorisation */ '');

FILE_SCHEMA (('AUTOMOTIVE_DESIGN { 1 0 10303 214 3 1 1 }'));
ENDSEC;

DATA;
#10=MECHANICAL_DESIGN_GEOMETRIC_PRESENTATION_REPRESENTATION('',(#305),#16598);
#227=SHAPE_REPRESENTATION_RELATIONSHIP('SRR','None',#16721,#251);
#251=ADVANCED_BREP_SHAPE_REPRESENTATION('',(#275),#16597);
#275=MANIFOLD_SOLID_BREP('Body1',#9810);
#305=STYLED_ITEM('',(#16831),#275);
#427=FACE_BOUND('',#2125,.T.);
#428=FACE_BOUND('',#2127,.T.);
#901=PLANE('',#10874);
#902=PLANE('',#10875);
#903=PLANE('',#10876);
#904=PLANE('',#10877);
#905=PLANE('',#10878);
#906=PLANE('',#10879);
#907=PLANE('',#10880);
#908=PLANE('',#10881);
#909=PLANE('',#10882);
#910=PLANE('',#10883);
#1450=FACE_OUTER_BOUND('',#2122,.T.);
#1451=FACE_OUTER_BOUND('',#2123,.T.);
#1452=FACE_OUTER_BOUND('',#2124,.T.);
#1453=FACE_OUTER_BOUND('',#2126,.T.);
#1454=FACE_OUTER_BOUND('',#2128,.T.);
#1455=FACE_OUTER_BOUND('',#2129,.T.);
#1456=FACE_OUTER_BOUND('',#2130,.T.);
#1457=FACE_OUTER_BOUND('',#2131,.T.);
#1458=FACE_OUTER_BOUND('',#2132,.T.);
#1459=FACE_OUTER_BOUND('',#2133,.T.);
#1460=FACE_OUTER_BOUND('',#2134,.T.);
#1461=FACE_OUTER_BOUND('',#2135,.T.);
#2122=EDGE_LOOP('',(#9121,#9122,#9123,#9124));
#2123=EDGE_LOOP('',(#9125,#9126,#9127,#9128));
#2124=EDGE_LOOP('',(#9129));
#2125=EDGE_LOOP('',(#9130,#9131,#9132,#9133,#9134,#9135));
#2126=EDGE_LOOP('',(#9136));
#2127=EDGE_LOOP('',(#9137));
#2128=EDGE_LOOP('',(#9138));
#2129=EDGE_LOOP('',(#9139,#9140,#9141,#9142));
#2130=EDGE_LOOP('',(#9143,#9144,#9145,#9146));
#2131=EDGE_LOOP('',(#9147,#9148,#9149,#9150));
#2132=EDGE_LOOP('',(#9151,#9152,#9153,#9154));
#2133=EDGE_LOOP('',(#9155,#9156,#9157,#9158));
#2134=EDGE_LOOP('',(#9159,#9160,#9161,#9162));
#2135=EDGE_LOOP('',(#9163,#9164,#9165,#9166,#9167,#9168));
#3164=LINE('',#16455,#4212);
#3165=LINE('',#16461,#4213);
#3166=LINE('',#16466,#4214);
#3167=LINE('',#16468,#4215);
#3168=LINE('',#16470,#4216);
#3169=LINE('',#16472,#4217);
#3170=LINE('',#16474,#4218);
#3171=LINE('',#16475,#4219);
#3172=LINE('',#16480,#4220);
#3173=LINE('',#16482,#4221);
#3174=LINE('',#16483,#4222);
#3175=LINE('',#16486,#4223);
#3176=LINE('',#16487,#4224);
#3177=LINE('',#16490,#4225);
#3178=LINE('',#16491,#4226);
#3179=LINE('',#16494,#4227);
#3180=LINE('',#16495,#4228);
#3181=LINE('',#16498,#4229);
#3182=LINE('',#16499,#4230);
#3183=LINE('',#16501,#4231);
#4212=VECTOR('',#13544,1.5);
#4213=VECTOR('',#13551,3.5);
#4214=VECTOR('',#13556,1000.);
#4215=VECTOR('',#13557,1000.);
#4216=VECTOR('',#13558,1000.);
#4217=VECTOR('',#13559,1000.);
#4218=VECTOR('',#13560,1000.);
#4219=VECTOR('',#13561,1000.);
#4220=VECTOR('',#13568,1000.);
#4221=VECTOR('',#13569,1000.);
#4222=VECTOR('',#13570,1000.);
#4223=VECTOR('',#13573,1000.);
#4224=VECTOR('',#13574,1000.);
#4225=VECTOR('',#13577,1000.);
#4226=VECTOR('',#13578,1000.);
#4227=VECTOR('',#13581,1000.);
#4228=VECTOR('',#13582,1000.);
#4229=VECTOR('',#13585,1000.);
#4230=VECTOR('',#13586,1000.);
#4231=VECTOR('',#13589,1000.);
#4451=CIRCLE('',#10869,1.5);
#4452=CIRCLE('',#10870,1.5);
#4453=CIRCLE('',#10872,3.5);
#4454=CIRCLE('',#10873,3.5);
#5295=VERTEX_POINT('',#16452);
#5296=VERTEX_POINT('',#16454);
#5297=VERTEX_POINT('',#16458);
#5298=VERTEX_POINT('',#16460);
#5299=VERTEX_POINT('',#16464);
#5300=VERTEX_POINT('',#16465);
#5301=VERTEX_POINT('',#16467);
#5302=VERTEX_POINT('',#16469);
#5303=VERTEX_POINT('',#16471);
#5304=VERTEX_POINT('',#16473);
#5305=VERTEX_POINT('',#16479);
#5306=VERTEX_POINT('',#16481);
#5307=VERTEX_POINT('',#16485);
#5308=VERTEX_POINT('',#16489);
#5309=VERTEX_POINT('',#16493);
#5310=VERTEX_POINT('',#16497);
#6573=EDGE_CURVE('',#5295,#5295,#4451,.T.);
#6574=EDGE_CURVE('',#5295,#5296,#3164,.T.);
#6575=EDGE_CURVE('',#5296,#5296,#4452,.T.);
#6576=EDGE_CURVE('',#5297,#5297,#4453,.T.);
#6577=EDGE_CURVE('',#5297,#5298,#3165,.T.);
#6578=EDGE_CURVE('',#5298,#5298,#4454,.T.);
#6579=EDGE_CURVE('',#5299,#5300,#3166,.T.);
#6580=EDGE_CURVE('',#5301,#5299,#3167,.T.);
#6581=EDGE_CURVE('',#5302,#5301,#3168,.T.);
#6582=EDGE_CURVE('',#5303,#5302,#3169,.T.);
#6583=EDGE_CURVE('',#5304,#5303,#3170,.T.);
#6584=EDGE_CURVE('',#5300,#5304,#3171,.T.);
#6585=EDGE_CURVE('',#5305,#5300,#3172,.T.);
#6586=EDGE_CURVE('',#5305,#5306,#3173,.T.);
#6587=EDGE_CURVE('',#5306,#5299,#3174,.T.);
#6588=EDGE_CURVE('',#5306,#5307,#3175,.T.);
#6589=EDGE_CURVE('',#5307,#5301,#3176,.T.);
#6590=EDGE_CURVE('',#5307,#5308,#3177,.T.);
#6591=EDGE_CURVE('',#5308,#5302,#3178,.T.);
#6592=EDGE_CURVE('',#5308,#5309,#3179,.T.);
#6593=EDGE_CURVE('',#5309,#5303,#3180,.T.);
#6594=EDGE_CURVE('',#5309,#5310,#3181,.T.);
#6595=EDGE_CURVE('',#5310,#5304,#3182,.T.);
#6596=EDGE_CURVE('',#5310,#5305,#3183,.T.);
#9121=ORIENTED_EDGE('',*,*,#6573,.T.);
#9122=ORIENTED_EDGE('',*,*,#6574,.T.);
#9123=ORIENTED_EDGE('',*,*,#6575,.F.);
#9124=ORIENTED_EDGE('',*,*,#6574,.F.);
#9125=ORIENTED_EDGE('',*,*,#6576,.T.);
#9126=ORIENTED_EDGE('',*,*,#6577,.T.);
#9127=ORIENTED_EDGE('',*,*,#6578,.F.);
#9128=ORIENTED_EDGE('',*,*,#6577,.F.);
#9129=ORIENTED_EDGE('',*,*,#6576,.F.);
#9130=ORIENTED_EDGE('',*,*,#6579,.F.);
#9131=ORIENTED_EDGE('',*,*,#6580,.F.);
#9132=ORIENTED_EDGE('',*,*,#6581,.F.);
#9133=ORIENTED_EDGE('',*,*,#6582,.F.);
#9134=ORIENTED_EDGE('',*,*,#6583,.F.);
#9135=ORIENTED_EDGE('',*,*,#6584,.F.);
#9136=ORIENTED_EDGE('',*,*,#6578,.T.);
#9137=ORIENTED_EDGE('',*,*,#6573,.F.);
#9138=ORIENTED_EDGE('',*,*,#6575,.T.);
#9139=ORIENTED_EDGE('',*,*,#6579,.T.);
#9140=ORIENTED_EDGE('',*,*,#6585,.F.);
#9141=ORIENTED_EDGE('',*,*,#6586,.T.);
#9142=ORIENTED_EDGE('',*,*,#6587,.T.);
#9143=ORIENTED_EDGE('',*,*,#6580,.T.);
#9144=ORIENTED_EDGE('',*,*,#6587,.F.);
#9145=ORIENTED_EDGE('',*,*,#6588,.T.);
#9146=ORIENTED_EDGE('',*,*,#6589,.T.);
#9147=ORIENTED_EDGE('',*,*,#6581,.T.);
#9148=ORIENTED_EDGE('',*,*,#6589,.F.);
#9149=ORIENTED_EDGE('',*,*,#6590,.T.);
#9150=ORIENTED_EDGE('',*,*,#6591,.T.);
#9151=ORIENTED_EDGE('',*,*,#6582,.T.);
#9152=ORIENTED_EDGE('',*,*,#6591,.F.);
#9153=ORIENTED_EDGE('',*,*,#6592,.T.);
#9154=ORIENTED_EDGE('',*,*,#6593,.T.);
#9155=ORIENTED_EDGE('',*,*,#6583,.T.);
#9156=ORIENTED_EDGE('',*,*,#6593,.F.);
#9157=ORIENTED_EDGE('',*,*,#6594,.T.);
#9158=ORIENTED_EDGE('',*,*,#6595,.T.);
#9159=ORIENTED_EDGE('',*,*,#6584,.T.);
#9160=ORIENTED_EDGE('',*,*,#6595,.F.);
#9161=ORIENTED_EDGE('',*,*,#6596,.T.);
#9162=ORIENTED_EDGE('',*,*,#6585,.T.);
#9163=ORIENTED_EDGE('',*,*,#6586,.F.);
#9164=ORIENTED_EDGE('',*,*,#6596,.F.);
#9165=ORIENTED_EDGE('',*,*,#6594,.F.);
#9166=ORIENTED_EDGE('',*,*,#6592,.F.);
#9167=ORIENTED_EDGE('',*,*,#6590,.F.);
#9168=ORIENTED_EDGE('',*,*,#6588,.F.);
#9234=CYLINDRICAL_SURFACE('',#10868,1.5);
#9235=CYLINDRICAL_SURFACE('',#10871,3.5);
#9775=ADVANCED_FACE('',(#1450),#9234,.T.);
#9776=ADVANCED_FACE('',(#1451),#9235,.T.);
#9777=ADVANCED_FACE('',(#1452,#427),#901,.F.);
#9778=ADVANCED_FACE('',(#1453,#428),#902,.T.);
#9779=ADVANCED_FACE('',(#1454),#903,.T.);
#9780=ADVANCED_FACE('',(#1455),#904,.T.);
#9781=ADVANCED_FACE('',(#1456),#905,.T.);
#9782=ADVANCED_FACE('',(#1457),#906,.T.);
#9783=ADVANCED_FACE('',(#1458),#907,.T.);
#9784=ADVANCED_FACE('',(#1459),#908,.T.);
#9785=ADVANCED_FACE('',(#1460),#909,.T.);
#9786=ADVANCED_FACE('',(#1461),#910,.F.);
#9810=CLOSED_SHELL('',(#9775,#9776,#9777,#9778,#9779,#9780,#9781,#9782,
#9783,#9784,#9785,#9786));
#10867=AXIS2_PLACEMENT_3D('',#16450,#13538,#13539);
#10868=AXIS2_PLACEMENT_3D('',#16451,#13540,#13541);
#10869=AXIS2_PLACEMENT_3D('',#16453,#13542,#13543);
#10870=AXIS2_PLACEMENT_3D('',#16456,#13545,#13546);
#10871=AXIS2_PLACEMENT_3D('',#16457,#13547,#13548);
#10872=AXIS2_PLACEMENT_3D('',#16459,#13549,#13550);
#10873=AXIS2_PLACEMENT_3D('',#16462,#13552,#13553);
#10874=AXIS2_PLACEMENT_3D('',#16463,#13554,#13555);
#10875=AXIS2_PLACEMENT_3D('',#16476,#13562,#13563);
#10876=AXIS2_PLACEMENT_3D('',#16477,#13564,#13565);
#10877=AXIS2_PLACEMENT_3D('',#16478,#13566,#13567);
#10878=AXIS2_PLACEMENT_3D('',#16484,#13571,#13572);
#10879=AXIS2_PLACEMENT_3D('',#16488,#13575,#13576);
#10880=AXIS2_PLACEMENT_3D('',#16492,#13579,#13580);
#10881=AXIS2_PLACEMENT_3D('',#16496,#13583,#13584);
#10882=AXIS2_PLACEMENT_3D('',#16500,#13587,#13588);
#10883=AXIS2_PLACEMENT_3D('',#16502,#13590,#13591);
#13538=DIRECTION('axis',(0.,0.,1.));
#13539=DIRECTION('refdir',(1.,0.,0.));
#13540=DIRECTION('center_axis',(0.,0.,-1.));
#13541=DIRECTION('ref_axis',(-1.,0.,0.));
#13542=DIRECTION('center_axis',(0.,0.,1.));
#13543=DIRECTION('ref_axis',(1.,0.,0.));
#13544=DIRECTION('',(0.,0.,1.));
#13545=DIRECTION('center_axis',(0.,0.,1.));
#13546=DIRECTION('ref_axis',(1.,0.,0.));
#13547=DIRECTION('center_axis',(0.,0.,-1.));
#13548=DIRECTION('ref_axis',(-1.,0.,0.));
#13549=DIRECTION('center_axis',(0.,0.,1.));
#13550=DIRECTION('ref_axis',(1.,0.,0.));
#13551=DIRECTION('',(0.,0.,1.));
#13552=DIRECTION('center_axis',(0.,0.,1.));
#13553=DIRECTION('ref_axis',(1.,0.,0.));
#13554=DIRECTION('center_axis',(0.,0.,1.));
#13555=DIRECTION('ref_axis',(1.,0.,0.));
#13556=DIRECTION('',(-0.5,-0.866025403784439,0.));
#13557=DIRECTION('',(0.5,-0.866025403784439,0.));
#13558=DIRECTION('',(1.,-1.50231459873716E-16,0.));
#13559=DIRECTION('',(0.5,0.866025403784438,0.));
#13560=DIRECTION('',(-0.5,0.866025403784439,0.));
#13561=DIRECTION('',(-1.,1.50231459873716E-16,0.));
#13562=DIRECTION('center_axis',(0.,0.,1.));
#13563=DIRECTION('ref_axis',(1.,0.,0.));
#13564=DIRECTION('center_axis',(0.,0.,1.));
#13565=DIRECTION('ref_axis',(1.,0.,0.));
#13566=DIRECTION('center_axis',(-0.866025403784439,0.5,0.));
#13567=DIRECTION('ref_axis',(-0.5,-0.866025403784439,0.));
#13568=DIRECTION('',(0.,0.,-1.));
#13569=DIRECTION('',(0.5,0.866025403784439,0.));
#13570=DIRECTION('',(0.,0.,-1.));
#13571=DIRECTION('center_axis',(-0.866025403784439,-0.5,0.));
#13572=DIRECTION('ref_axis',(0.5,-0.866025403784439,0.));
#13573=DIRECTION('',(-0.5,0.866025403784439,0.));
#13574=DIRECTION('',(0.,0.,-1.));
#13575=DIRECTION('center_axis',(-1.50231459873716E-16,-1.,0.));
#13576=DIRECTION('ref_axis',(1.,-1.50231459873716E-16,0.));
#13577=DIRECTION('',(-1.,1.50231459873716E-16,0.));
#13578=DIRECTION('',(0.,0.,-1.));
#13579=DIRECTION('center_axis',(0.866025403784439,-0.5,0.));
#13580=DIRECTION('ref_axis',(0.5,0.866025403784439,0.));
#13581=DIRECTION('',(-0.5,-0.866025403784438,0.));
#13582=DIRECTION('',(0.,0.,-1.));
#13583=DIRECTION('center_axis',(0.866025403784439,0.5,0.));
#13584=DIRECTION('ref_axis',(-0.5,0.866025403784439,0.));
#13585=DIRECTION('',(0.5,-0.866025403784439,0.));
#13586=DIRECTION('',(0.,0.,-1.));
#13587=DIRECTION('center_axis',(1.50231459873716E-16,1.,0.));
#13588=DIRECTION('ref_axis',(-1.,1.50231459873716E-16,0.));
#13589=DIRECTION('',(1.,-1.50231459873716E-16,0.));
#13590=DIRECTION('center_axis',(0.,0.,1.));
#13591=DIRECTION('ref_axis',(1.,0.,0.));
#16450=CARTESIAN_POINT('',(0.,0.,0.));
#16451=CARTESIAN_POINT('Origin',(0.,0.,12.));
#16452=CARTESIAN_POINT('',(1.5,-1.83697019872103E-16,2.));
#16453=CARTESIAN_POINT('Origin',(0.,0.,2.));
#16454=CARTESIAN_POINT('',(1.5,-1.83697019872103E-16,12.));
#16455=CARTESIAN_POINT('',(1.5,-1.83697019872103E-16,12.));
#16456=CARTESIAN_POINT('Origin',(0.,0.,12.));
#16457=CARTESIAN_POINT('Origin',(0.,0.,2.));
#16458=CARTESIAN_POINT('',(3.5,-4.28626379701574E-16,0.));
#16459=CARTESIAN_POINT('Origin',(0.,0.,0.));
#16460=CARTESIAN_POINT('',(3.5,-4.28626379701574E-16,2.));
#16461=CARTESIAN_POINT('',(3.5,-4.28626379701574E-16,2.));
#16462=CARTESIAN_POINT('Origin',(0.,0.,2.));
#16463=CARTESIAN_POINT('Origin',(0.,0.,0.));
#16464=CARTESIAN_POINT('',(1.44337567297406,0.,0.));
#16465=CARTESIAN_POINT('',(0.721687836487032,-1.25,0.));
#16466=CARTESIAN_POINT('',(1.08253175473055,-0.625,0.));
#16467=CARTESIAN_POINT('',(0.721687836487032,1.25,0.));
#16468=CARTESIAN_POINT('',(1.08253175473055,0.625,0.));
#16469=CARTESIAN_POINT('',(-0.721687836487032,1.25,0.));
#16470=CARTESIAN_POINT('',(1.87789324842145E-16,1.25,0.));
#16471=CARTESIAN_POINT('',(-1.44337567297406,1.76762539787484E-16,0.));
#16472=CARTESIAN_POINT('',(-1.08253175473055,0.625,0.));
#16473=CARTESIAN_POINT('',(-0.721687836487033,-1.25,0.));
#16474=CARTESIAN_POINT('',(-1.08253175473055,-0.625,0.));
#16475=CARTESIAN_POINT('',(-1.87789324842145E-16,-1.25,0.));
#16476=CARTESIAN_POINT('Origin',(0.,0.,2.));
#16477=CARTESIAN_POINT('Origin',(0.,0.,12.));
#16478=CARTESIAN_POINT('Origin',(0.721687836487032,-1.25,1.3));
#16479=CARTESIAN_POINT('',(0.721687836487032,-1.25,1.3));
#16480=CARTESIAN_POINT('',(0.721687836487032,-1.25,1.3));
#16481=CARTESIAN_POINT('',(1.44337567297406,0.,1.3));
#16482=CARTESIAN_POINT('',(0.721687836487032,-1.25,1.3));
#16483=CARTESIAN_POINT('',(1.44337567297406,0.,1.3));
#16484=CARTESIAN_POINT('Origin',(1.44337567297406,0.,1.3));
#16485=CARTESIAN_POINT('',(0.721687836487032,1.25,1.3));
#16486=CARTESIAN_POINT('',(1.44337567297406,0.,1.3));
#16487=CARTESIAN_POINT('',(0.721687836487032,1.25,1.3));
#16488=CARTESIAN_POINT('Origin',(0.721687836487032,1.25,1.3));
#16489=CARTESIAN_POINT('',(-0.721687836487032,1.25,1.3));
#16490=CARTESIAN_POINT('',(0.721687836487032,1.25,1.3));
#16491=CARTESIAN_POINT('',(-0.721687836487032,1.25,1.3));
#16492=CARTESIAN_POINT('Origin',(-0.721687836487032,1.25,1.3));
#16493=CARTESIAN_POINT('',(-1.44337567297406,1.76762539787484E-16,1.3));
#16494=CARTESIAN_POINT('',(-0.721687836487032,1.25,1.3));
#16495=CARTESIAN_POINT('',(-1.44337567297406,1.76762539787484E-16,1.3));
#16496=CARTESIAN_POINT('Origin',(-1.44337567297406,1.76762539787484E-16,
1.3));
#16497=CARTESIAN_POINT('',(-0.721687836487033,-1.25,1.3));
#16498=CARTESIAN_POINT('',(-1.44337567297406,1.76762539787484E-16,1.3));
#16499=CARTESIAN_POINT('',(-0.721687836487033,-1.25,1.3));
#16500=CARTESIAN_POINT('Origin',(-0.721687836487033,-1.25,1.3));
#16501=CARTESIAN_POINT('',(-0.721687836487033,-1.25,1.3));
#16502=CARTESIAN_POINT('Origin',(0.,0.,1.3));
#16571=UNCERTAINTY_MEASURE_WITH_UNIT(LENGTH_MEASURE(0.01),#16599,
'DISTANCE_ACCURACY_VALUE',
'Maximum model space distance between geometric entities at asserted c
onnectivities');
#16572=UNCERTAINTY_MEASURE_WITH_UNIT(LENGTH_MEASURE(0.01),#16599,
'DISTANCE_ACCURACY_VALUE',
'Maximum model space distance between geometric entities at asserted c
onnectivities');
#16597=(
GEOMETRIC_REPRESENTATION_CONTEXT(3)
GLOBAL_UNCERTAINTY_ASSIGNED_CONTEXT((#16571))
GLOBAL_UNIT_ASSIGNED_CONTEXT((#16599,#16601,#16602))
REPRESENTATION_CONTEXT('','3D')
);
#16598=(
GEOMETRIC_REPRESENTATION_CONTEXT(3)
GLOBAL_UNCERTAINTY_ASSIGNED_CONTEXT((#16572))
GLOBAL_UNIT_ASSIGNED_CONTEXT((#16599,#16601,#16602))
REPRESENTATION_CONTEXT('','3D')
);
#16599=(
LENGTH_UNIT()
NAMED_UNIT(*)
SI_UNIT(.MILLI.,.METRE.)
);
#16601=(
NAMED_UNIT(*)
PLANE_ANGLE_UNIT()
SI_UNIT($,.RADIAN.)
);
#16602=(
NAMED_UNIT(*)
SI_UNIT($,.STERADIAN.)
SOLID_ANGLE_UNIT()
);
#16627=SHAPE_DEFINITION_REPRESENTATION(#16652,#16721);
#16652=PRODUCT_DEFINITION_SHAPE('',$,#16747);
#16721=SHAPE_REPRESENTATION('',(#10867),#16597);
#16722=PRODUCT_DEFINITION_CONTEXT('part definition',#16799,'design');
#16747=PRODUCT_DEFINITION('F06_M4x10_Retainer_Screw',
'F06_M4x10_Retainer_Screw',#16772,#16722);
#16772=PRODUCT_DEFINITION_FORMATION('',$,#16825);
#16799=APPLICATION_CONTEXT(
'Core Data for Automotive Mechanical Design Process');
#16800=PRODUCT_CONTEXT('part definition',#16799,'mechanical');
#16825=PRODUCT('F06_M4x10_Retainer_Screw','F06_M4x10_Retainer_Screw',$,
(#16800));
#16831=PRESENTATION_STYLE_ASSIGNMENT((#16840));
#16840=SURFACE_STYLE_USAGE(.BOTH.,#16849);
#16849=SURFACE_SIDE_STYLE('',(#16858));
#16858=SURFACE_STYLE_FILL_AREA(#16867);
#16867=FILL_AREA_STYLE('Black',(#16876));
#16876=FILL_AREA_STYLE_COLOUR('Black',#16885);
#16885=COLOUR_RGB('Black',0.0784313725490196,0.0784313725490196,0.0784313725490196);
ENDSEC;
END-ISO-10303-21;
